ISO-10303-21;
HEADER;
/* Generated by software containing ST-Developer
 * from STEP Tools, Inc. (www.steptools.com) 
 */

FILE_DESCRIPTION(
/* description */ (''),
/* implementation_level */ '2;1');

FILE_NAME(
/* name */ '05_O-Ring_30x3.1_NBR.step',
/* time_stamp */ '2026-10-26T03:55:20-07:00',
/* author */ (''),
/* organization */ (''),
/* preprocessor_version */ 'ST-DEVELOPER v20.2',
/* originating_system */ 'Autodesk Translation Framework v15.15.0.0',
/* authorisation */ '');

FILE_SCHEMA (('AUTOMOTIVE_DESIGN { 1 0 10303 214 3 1 1 }'));
ENDSEC;

DATA;
#10=MECHANICAL_DESIGN_GEOMETRIC_PRESENTATION_REPRESENTATION('',(#179),#45236);
#139=SHAPE_REPRESENTATION_RELATIONSHIP('SRR','None',#45318,#159);
#159=ADVANCED_BREP_SHAPE_REPRESENTATION('',(#199),#45220);
#179=STYLED_ITEM('',(#45491),#199);
#199=MANIFOLD_SOLID_BREP('Body1',#16521);
#224=TOROIDAL_SURFACE('',#17153,16.52,1.465);
#2091=FACE_OUTER_BOUND('',#3089,.T.);
#3089=EDGE_LOOP('',(#12134,#12135,#12136,#12137));
#6663=CIRCLE('',#17154,1.465);
#6664=CIRCLE('',#17155,15.055);
#7379=VERTEX_POINT('',#32229);
#9130=EDGE_CURVE('',#7379,#7379,#6663,.T.);
#9131=EDGE_CURVE('',#7379,#7379,#6664,.T.);
#12134=ORIENTED_EDGE('',*,*,#9130,.F.);
#12135=ORIENTED_EDGE('',*,*,#9131,.T.);
#12136=ORIENTED_EDGE('',*,*,#9130,.T.);
#12137=ORIENTED_EDGE('',*,*,#9131,.F.);
#15819=ADVANCED_FACE('',(#2091),#224,.T.);
#16521=CLOSED_SHELL('',(#15819));
#17152=AXIS2_PLACEMENT_3D('',#32227,#19191,#19192);
#17153=AXIS2_PLACEMENT_3D('',#32228,#19193,#19194);
#17154=AXIS2_PLACEMENT_3D('',#32230,#19195,#19196);
#17155=AXIS2_PLACEMENT_3D('',#32231,#19197,#19198);
#19191=DIRECTION('axis',(0.,0.,1.));
#19192=DIRECTION('refdir',(1.,0.,0.));
#19193=DIRECTION('center_axis',(1.,0.,0.));
#19194=DIRECTION('ref_axis',(0.,0.,-1.));
#19195=DIRECTION('center_axis',(0.,-1.,-1.22464679914735E-16));
#19196=DIRECTION('ref_axis',(0.,-1.22464679914735E-16,1.));
#19197=DIRECTION('center_axis',(-1.,0.,0.));
#19198=DIRECTION('ref_axis',(0.,0.,-1.));
#32227=CARTESIAN_POINT('',(0.,0.,0.));
#32228=CARTESIAN_POINT('Origin',(0.,0.,0.));
#32229=CARTESIAN_POINT('',(1.79410756075087E-16,-1.84370575611634E-15,15.055));
#32230=CARTESIAN_POINT('Origin',(0.,-2.02311651219143E-15,16.52));
#32231=CARTESIAN_POINT('Origin',(-1.79410756075087E-16,0.,0.));
#45198=UNCERTAINTY_MEASURE_WITH_UNIT(LENGTH_MEASURE(0.01),#45237,
'DISTANCE_ACCURACY_VALUE',
'Maximum model space distance between geometric entities at asserted c
onnectivities');
#45214=UNCERTAINTY_MEASURE_WITH_UNIT(LENGTH_MEASURE(0.01),#45237,
'DISTANCE_ACCURACY_VALUE',
'Maximum model space distance between geometric entities at asserted c
onnectivities');
#45220=(
GEOMETRIC_REPRESENTATION_CONTEXT(3)
GLOBAL_UNCERTAINTY_ASSIGNED_CONTEXT((#45198))
GLOBAL_UNIT_ASSIGNED_CONTEXT((#45237,#45239,#45240))
REPRESENTATION_CONTEXT('','3D')
);
#45236=(
GEOMETRIC_REPRESENTATION_CONTEXT(3)
GLOBAL_UNCERTAINTY_ASSIGNED_CONTEXT((#45214))
GLOBAL_UNIT_ASSIGNED_CONTEXT((#45237,#45239,#45240))
REPRESENTATION_CONTEXT('','3D')
);
#45237=(
LENGTH_UNIT()
NAMED_UNIT(*)
SI_UNIT(.MILLI.,.METRE.)
);
#45239=(
NAMED_UNIT(*)
PLANE_ANGLE_UNIT()
SI_UNIT($,.RADIAN.)
);
#45240=(
NAMED_UNIT(*)
SI_UNIT($,.STERADIAN.)
SOLID_ANGLE_UNIT()
);
#45246=SHAPE_DEFINITION_REPRESENTATION(#45267,#45318);
#45267=PRODUCT_DEFINITION_SHAPE('',$,#45340);
#45318=SHAPE_REPRESENTATION('',(#17152),#45220);
#45334=PRODUCT_DEFINITION_CONTEXT('part definition',#45399,'design');
#45340=PRODUCT_DEFINITION('2026-10-25-23-38-16-850',
'05_O-Ring_30x3.1_NBR',#45361,#45334);
#45361=PRODUCT_DEFINITION_FORMATION('',$,#45406);
#45399=APPLICATION_CONTEXT(
'Core Data for Automotive Mechanical Design Process');
#45400=PRODUCT_CONTEXT('part definition',#45399,'mechanical');
#45406=PRODUCT('2026-10-25-23-38-16-850','05_O-Ring_30x3.1_NBR',$,(#45400));
#45485=COLOUR_RGB('Black',0.12,0.14,0.17);
#45486=FILL_AREA_STYLE_COLOUR('',#45485);
#45487=FILL_AREA_STYLE('',(#45486));
#45488=SURFACE_STYLE_FILL_AREA(#45487);
#45489=SURFACE_SIDE_STYLE('',(#45488));
#45490=SURFACE_STYLE_USAGE(.BOTH.,#45489);
#45491=PRESENTATION_STYLE_ASSIGNMENT((#45490));
ENDSEC;
END-ISO-10303-21;
